ISO-10303-21;
HEADER;
/* Generated by software containing ST-Developer
 * from STEP Tools, Inc. (www.steptools.com) 
 */

FILE_DESCRIPTION(
/* description */ ('Worm-less right-angle friction wheel drive'),
/* implementation_level */ '2;1');

FILE_NAME(
/* name */ 'Hex Nut - M6.step',
/* time_stamp */ '2026-10-28T03:22:36-07:00',
/* author */ (''),
/* organization */ (''),
/* preprocessor_version */ 'ST-DEVELOPER v20.2',
/* originating_system */ 'Autodesk Translation Framework v15.17.0.0',
/* authorisation */ '');

FILE_SCHEMA (('AUTOMOTIVE_DESIGN { 1 0 10303 214 3 1 1 }'));
ENDSEC;

DATA;
#10=MECHANICAL_DESIGN_GEOMETRIC_PRESENTATION_REPRESENTATION('',(#649),#17046);
#11=(
BOUNDED_CURVE()
B_SPLINE_CURVE(2,(#16060,#16061,#16062),.UNSPECIFIED.,.F.,.F.)
B_SPLINE_CURVE_WITH_KNOTS((3,3),(0.144988513094728,0.791574906712449),
 .UNSPECIFIED.)
CURVE()
GEOMETRIC_REPRESENTATION_ITEM()
RATIONAL_B_SPLINE_CURVE((1.09282032302755,1.26188021535082,1.09282032302931))
REPRESENTATION_ITEM('')
);
#12=(
BOUNDED_CURVE()
B_SPLINE_CURVE(2,(#16064,#16065,#16066),.UNSPECIFIED.,.F.,.F.)
B_SPLINE_CURVE_WITH_KNOTS((3,3),(0.144988513094728,0.791574906712449),
 .UNSPECIFIED.)
CURVE()
GEOMETRIC_REPRESENTATION_ITEM()
RATIONAL_B_SPLINE_CURVE((1.09282032302755,1.26188021535082,1.09282032302931))
REPRESENTATION_ITEM('')
);
#13=(
BOUNDED_CURVE()
B_SPLINE_CURVE(2,(#16071,#16072,#16073),.UNSPECIFIED.,.F.,.F.)
B_SPLINE_CURVE_WITH_KNOTS((3,3),(0.144988513094728,0.791574906712449),
 .UNSPECIFIED.)
CURVE()
GEOMETRIC_REPRESENTATION_ITEM()
RATIONAL_B_SPLINE_CURVE((1.09282032302755,1.26188021535082,1.09282032302931))
REPRESENTATION_ITEM('')
);
#14=(
BOUNDED_CURVE()
B_SPLINE_CURVE(2,(#16075,#16076,#16077),.UNSPECIFIED.,.F.,.F.)
B_SPLINE_CURVE_WITH_KNOTS((3,3),(0.144988513094728,0.791574906712449),
 .UNSPECIFIED.)
CURVE()
GEOMETRIC_REPRESENTATION_ITEM()
RATIONAL_B_SPLINE_CURVE((1.09282032302755,1.26188021535082,1.09282032302931))
REPRESENTATION_ITEM('')
);
#15=(
BOUNDED_CURVE()
B_SPLINE_CURVE(2,(#16079,#16080,#16081),.UNSPECIFIED.,.F.,.F.)
B_SPLINE_CURVE_WITH_KNOTS((3,3),(0.144988513094728,0.791574906712449),
 .UNSPECIFIED.)
CURVE()
GEOMETRIC_REPRESENTATION_ITEM()
RATIONAL_B_SPLINE_CURVE((1.09282032302755,1.26188021535082,1.09282032302931))
REPRESENTATION_ITEM('')
);
#16=(
BOUNDED_CURVE()
B_SPLINE_CURVE(2,(#16082,#16083,#16084),.UNSPECIFIED.,.F.,.F.)
B_SPLINE_CURVE_WITH_KNOTS((3,3),(0.144988513094728,0.791574906712449),
 .UNSPECIFIED.)
CURVE()
GEOMETRIC_REPRESENTATION_ITEM()
RATIONAL_B_SPLINE_CURVE((1.09282032302755,1.26188021535082,1.09282032302931))
REPRESENTATION_ITEM('')
);
#17=(
BOUNDED_CURVE()
B_SPLINE_CURVE(2,(#16091,#16092,#16093),.UNSPECIFIED.,.F.,.F.)
B_SPLINE_CURVE_WITH_KNOTS((3,3),(0.144988513094728,0.791574906712449),
 .UNSPECIFIED.)
CURVE()
GEOMETRIC_REPRESENTATION_ITEM()
RATIONAL_B_SPLINE_CURVE((1.09282032302755,1.26188021535082,1.09282032302931))
REPRESENTATION_ITEM('')
);
#18=(
BOUNDED_CURVE()
B_SPLINE_CURVE(2,(#16095,#16096,#16097),.UNSPECIFIED.,.F.,.F.)
B_SPLINE_CURVE_WITH_KNOTS((3,3),(0.144988513094727,0.791574906712449),
 .UNSPECIFIED.)
CURVE()
GEOMETRIC_REPRESENTATION_ITEM()
RATIONAL_B_SPLINE_CURVE((1.09282032302755,1.26188021535082,1.09282032302931))
REPRESENTATION_ITEM('')
);
#19=(
BOUNDED_CURVE()
B_SPLINE_CURVE(2,(#16099,#16100,#16101),.UNSPECIFIED.,.F.,.F.)
B_SPLINE_CURVE_WITH_KNOTS((3,3),(0.144988513094728,0.791574906712449),
 .UNSPECIFIED.)
CURVE()
GEOMETRIC_REPRESENTATION_ITEM()
RATIONAL_B_SPLINE_CURVE((1.09282032302755,1.26188021535082,1.09282032302931))
REPRESENTATION_ITEM('')
);
#20=(
BOUNDED_CURVE()
B_SPLINE_CURVE(2,(#16103,#16104,#16105),.UNSPECIFIED.,.F.,.F.)
B_SPLINE_CURVE_WITH_KNOTS((3,3),(0.144988513094728,0.791574906712449),
 .UNSPECIFIED.)
CURVE()
GEOMETRIC_REPRESENTATION_ITEM()
RATIONAL_B_SPLINE_CURVE((1.09282032302755,1.26188021535082,1.09282032302931))
REPRESENTATION_ITEM('')
);
#21=(
BOUNDED_CURVE()
B_SPLINE_CURVE(2,(#16107,#16108,#16109),.UNSPECIFIED.,.F.,.F.)
B_SPLINE_CURVE_WITH_KNOTS((3,3),(0.144988513094728,0.791574906712449),
 .UNSPECIFIED.)
CURVE()
GEOMETRIC_REPRESENTATION_ITEM()
RATIONAL_B_SPLINE_CURVE((1.09282032302755,1.26188021535082,1.09282032302931))
REPRESENTATION_ITEM('')
);
#22=(
BOUNDED_CURVE()
B_SPLINE_CURVE(2,(#16110,#16111,#16112),.UNSPECIFIED.,.F.,.F.)
B_SPLINE_CURVE_WITH_KNOTS((3,3),(0.144988513094727,0.791574906712449),
 .UNSPECIFIED.)
CURVE()
GEOMETRIC_REPRESENTATION_ITEM()
RATIONAL_B_SPLINE_CURVE((1.09282032302755,1.26188021535082,1.09282032302931))
REPRESENTATION_ITEM('')
);
#470=CONICAL_SURFACE('',#9440,0.576175134594813,1.0471975511966);
#471=CONICAL_SURFACE('',#9442,0.576175134594813,1.0471975511966);
#548=SHAPE_REPRESENTATION_RELATIONSHIP('SRR','None',#17292,#595);
#595=ADVANCED_BREP_SHAPE_REPRESENTATION('',(#700),#17028);
#649=STYLED_ITEM('',(#17598),#700);
#700=MANIFOLD_SOLID_BREP('Body1',#8207);
#917=FACE_BOUND('',#2218,.T.);
#918=FACE_BOUND('',#2220,.T.);
#1117=PLANE('',#9444);
#1118=PLANE('',#9445);
#1119=PLANE('',#9446);
#1120=PLANE('',#9450);
#1121=PLANE('',#9451);
#1122=PLANE('',#9452);
#1123=PLANE('',#9453);
#1124=PLANE('',#9454);
#1540=FACE_OUTER_BOUND('',#2208,.T.);
#1541=FACE_OUTER_BOUND('',#2209,.T.);
#1542=FACE_OUTER_BOUND('',#2210,.T.);
#1543=FACE_OUTER_BOUND('',#2211,.T.);
#1544=FACE_OUTER_BOUND('',#2212,.T.);
#1545=FACE_OUTER_BOUND('',#2213,.T.);
#1546=FACE_OUTER_BOUND('',#2214,.T.);
#1547=FACE_OUTER_BOUND('',#2215,.T.);
#1548=FACE_OUTER_BOUND('',#2216,.T.);
#1549=FACE_OUTER_BOUND('',#2217,.T.);
#1550=FACE_OUTER_BOUND('',#2219,.T.);
#2208=EDGE_LOOP('',(#6988,#6989,#6990,#6991,#6992,#6993,#6994,#6995,#6996));
#2209=EDGE_LOOP('',(#6997,#6998,#6999,#7000,#7001,#7002,#7003,#7004,#7005));
#2210=EDGE_LOOP('',(#7006,#7007,#7008,#7009));
#2211=EDGE_LOOP('',(#7010,#7011,#7012,#7013));
#2212=EDGE_LOOP('',(#7014,#7015,#7016,#7017));
#2213=EDGE_LOOP('',(#7018,#7019,#7020,#7021));
#2214=EDGE_LOOP('',(#7022,#7023,#7024,#7025));
#2215=EDGE_LOOP('',(#7026,#7027,#7028,#7029));
#2216=EDGE_LOOP('',(#7030,#7031,#7032,#7033));
#2217=EDGE_LOOP('',(#7034));
#2218=EDGE_LOOP('',(#7035));
#2219=EDGE_LOOP('',(#7036));
#2220=EDGE_LOOP('',(#7037));
#2760=LINE('',#16068,#3300);
#2761=LINE('',#16089,#3301);
#2762=LINE('',#16114,#3302);
#2763=LINE('',#16115,#3303);
#2764=LINE('',#16117,#3304);
#2765=LINE('',#16119,#3305);
#2766=LINE('',#16124,#3306);
#2767=LINE('',#16127,#3307);
#2768=LINE('',#16129,#3308);
#3300=VECTOR('',#11554,0.576175134594813);
#3301=VECTOR('',#11561,0.576175134594813);
#3302=VECTOR('',#11564,1.);
#3303=VECTOR('',#11565,1.);
#3304=VECTOR('',#11568,1.);
#3305=VECTOR('',#11571,1.);
#3306=VECTOR('',#11576,0.3);
#3307=VECTOR('',#11581,1.);
#3308=VECTOR('',#11584,1.);
#3785=CIRCLE('',#9441,0.475);
#3786=CIRCLE('',#9443,0.475);
#3787=CIRCLE('',#9448,0.25175);
#3788=CIRCLE('',#9449,0.25175);
#4358=VERTEX_POINT('',#16058);
#4359=VERTEX_POINT('',#16059);
#4360=VERTEX_POINT('',#16063);
#4361=VERTEX_POINT('',#16067);
#4362=VERTEX_POINT('',#16070);
#4363=VERTEX_POINT('',#16074);
#4364=VERTEX_POINT('',#16078);
#4365=VERTEX_POINT('',#16086);
#4366=VERTEX_POINT('',#16088);
#4367=VERTEX_POINT('',#16090);
#4368=VERTEX_POINT('',#16094);
#4369=VERTEX_POINT('',#16098);
#4370=VERTEX_POINT('',#16102);
#4371=VERTEX_POINT('',#16106);
#4372=VERTEX_POINT('',#16121);
#4373=VERTEX_POINT('',#16123);
#5263=EDGE_CURVE('',#4358,#4359,#11,.T.);
#5264=EDGE_CURVE('',#4360,#4358,#12,.T.);
#5265=EDGE_CURVE('',#4360,#4361,#2760,.T.);
#5266=EDGE_CURVE('',#4361,#4361,#3785,.T.);
#5267=EDGE_CURVE('',#4362,#4360,#13,.T.);
#5268=EDGE_CURVE('',#4363,#4362,#14,.T.);
#5269=EDGE_CURVE('',#4364,#4363,#15,.T.);
#5270=EDGE_CURVE('',#4359,#4364,#16,.T.);
#5271=EDGE_CURVE('',#4365,#4365,#3786,.T.);
#5272=EDGE_CURVE('',#4365,#4366,#2761,.T.);
#5273=EDGE_CURVE('',#4367,#4366,#17,.T.);
#5274=EDGE_CURVE('',#4368,#4367,#18,.T.);
#5275=EDGE_CURVE('',#4369,#4368,#19,.T.);
#5276=EDGE_CURVE('',#4370,#4369,#20,.T.);
#5277=EDGE_CURVE('',#4371,#4370,#21,.T.);
#5278=EDGE_CURVE('',#4366,#4371,#22,.T.);
#5279=EDGE_CURVE('',#4362,#4371,#2762,.T.);
#5280=EDGE_CURVE('',#4363,#4370,#2763,.T.);
#5281=EDGE_CURVE('',#4360,#4366,#2764,.T.);
#5282=EDGE_CURVE('',#4358,#4367,#2765,.T.);
#5283=EDGE_CURVE('',#4372,#4372,#3787,.F.);
#5284=EDGE_CURVE('',#4372,#4373,#2766,.T.);
#5285=EDGE_CURVE('',#4373,#4373,#3788,.F.);
#5286=EDGE_CURVE('',#4359,#4368,#2767,.T.);
#5287=EDGE_CURVE('',#4364,#4369,#2768,.T.);
#6988=ORIENTED_EDGE('',*,*,#5263,.F.);
#6989=ORIENTED_EDGE('',*,*,#5264,.F.);
#6990=ORIENTED_EDGE('',*,*,#5265,.T.);
#6991=ORIENTED_EDGE('',*,*,#5266,.F.);
#6992=ORIENTED_EDGE('',*,*,#5265,.F.);
#6993=ORIENTED_EDGE('',*,*,#5267,.F.);
#6994=ORIENTED_EDGE('',*,*,#5268,.F.);
#6995=ORIENTED_EDGE('',*,*,#5269,.F.);
#6996=ORIENTED_EDGE('',*,*,#5270,.F.);
#6997=ORIENTED_EDGE('',*,*,#5271,.F.);
#6998=ORIENTED_EDGE('',*,*,#5272,.T.);
#6999=ORIENTED_EDGE('',*,*,#5273,.F.);
#7000=ORIENTED_EDGE('',*,*,#5274,.F.);
#7001=ORIENTED_EDGE('',*,*,#5275,.F.);
#7002=ORIENTED_EDGE('',*,*,#5276,.F.);
#7003=ORIENTED_EDGE('',*,*,#5277,.F.);
#7004=ORIENTED_EDGE('',*,*,#5278,.F.);
#7005=ORIENTED_EDGE('',*,*,#5272,.F.);
#7006=ORIENTED_EDGE('',*,*,#5268,.T.);
#7007=ORIENTED_EDGE('',*,*,#5279,.T.);
#7008=ORIENTED_EDGE('',*,*,#5277,.T.);
#7009=ORIENTED_EDGE('',*,*,#5280,.F.);
#7010=ORIENTED_EDGE('',*,*,#5267,.T.);
#7011=ORIENTED_EDGE('',*,*,#5281,.T.);
#7012=ORIENTED_EDGE('',*,*,#5278,.T.);
#7013=ORIENTED_EDGE('',*,*,#5279,.F.);
#7014=ORIENTED_EDGE('',*,*,#5264,.T.);
#7015=ORIENTED_EDGE('',*,*,#5282,.T.);
#7016=ORIENTED_EDGE('',*,*,#5273,.T.);
#7017=ORIENTED_EDGE('',*,*,#5281,.F.);
#7018=ORIENTED_EDGE('',*,*,#5283,.F.);
#7019=ORIENTED_EDGE('',*,*,#5284,.T.);
#7020=ORIENTED_EDGE('',*,*,#5285,.T.);
#7021=ORIENTED_EDGE('',*,*,#5284,.F.);
#7022=ORIENTED_EDGE('',*,*,#5263,.T.);
#7023=ORIENTED_EDGE('',*,*,#5286,.T.);
#7024=ORIENTED_EDGE('',*,*,#5274,.T.);
#7025=ORIENTED_EDGE('',*,*,#5282,.F.);
#7026=ORIENTED_EDGE('',*,*,#5269,.T.);
#7027=ORIENTED_EDGE('',*,*,#5280,.T.);
#7028=ORIENTED_EDGE('',*,*,#5276,.T.);
#7029=ORIENTED_EDGE('',*,*,#5287,.F.);
#7030=ORIENTED_EDGE('',*,*,#5270,.T.);
#7031=ORIENTED_EDGE('',*,*,#5287,.T.);
#7032=ORIENTED_EDGE('',*,*,#5275,.T.);
#7033=ORIENTED_EDGE('',*,*,#5286,.F.);
#7034=ORIENTED_EDGE('',*,*,#5271,.T.);
#7035=ORIENTED_EDGE('',*,*,#5283,.T.);
#7036=ORIENTED_EDGE('',*,*,#5266,.T.);
#7037=ORIENTED_EDGE('',*,*,#5285,.F.);
#7664=CYLINDRICAL_SURFACE('',#9447,0.25175);
#8032=ADVANCED_FACE('',(#1540),#470,.T.);
#8033=ADVANCED_FACE('',(#1541),#471,.T.);
#8034=ADVANCED_FACE('',(#1542),#1117,.T.);
#8035=ADVANCED_FACE('',(#1543),#1118,.T.);
#8036=ADVANCED_FACE('',(#1544),#1119,.T.);
#8037=ADVANCED_FACE('',(#1545),#7664,.F.);
#8038=ADVANCED_FACE('',(#1546),#1120,.T.);
#8039=ADVANCED_FACE('',(#1547),#1121,.T.);
#8040=ADVANCED_FACE('',(#1548),#1122,.T.);
#8041=ADVANCED_FACE('',(#1549,#917),#1123,.T.);
#8042=ADVANCED_FACE('',(#1550,#918),#1124,.F.);
#8207=CLOSED_SHELL('',(#8032,#8033,#8034,#8035,#8036,#8037,#8038,#8039,
#8040,#8041,#8042));
#9439=AXIS2_PLACEMENT_3D('',#16056,#11550,#11551);
#9440=AXIS2_PLACEMENT_3D('',#16057,#11552,#11553);
#9441=AXIS2_PLACEMENT_3D('',#16069,#11555,#11556);
#9442=AXIS2_PLACEMENT_3D('',#16085,#11557,#11558);
#9443=AXIS2_PLACEMENT_3D('',#16087,#11559,#11560);
#9444=AXIS2_PLACEMENT_3D('',#16113,#11562,#11563);
#9445=AXIS2_PLACEMENT_3D('',#16116,#11566,#11567);
#9446=AXIS2_PLACEMENT_3D('',#16118,#11569,#11570);
#9447=AXIS2_PLACEMENT_3D('',#16120,#11572,#11573);
#9448=AXIS2_PLACEMENT_3D('',#16122,#11574,#11575);
#9449=AXIS2_PLACEMENT_3D('',#16125,#11577,#11578);
#9450=AXIS2_PLACEMENT_3D('',#16126,#11579,#11580);
#9451=AXIS2_PLACEMENT_3D('',#16128,#11582,#11583);
#9452=AXIS2_PLACEMENT_3D('',#16130,#11585,#11586);
#9453=AXIS2_PLACEMENT_3D('',#16131,#11587,#11588);
#9454=AXIS2_PLACEMENT_3D('',#16132,#11589,#11590);
#11550=DIRECTION('axis',(0.,0.,1.));
#11551=DIRECTION('refdir',(1.,0.,0.));
#11552=DIRECTION('center_axis',(0.,1.,0.));
#11553=DIRECTION('ref_axis',(1.,0.,0.));
#11554=DIRECTION('',(0.866025403784439,-0.5,1.06057523872491E-16));
#11555=DIRECTION('center_axis',(0.,-1.,0.));
#11556=DIRECTION('ref_axis',(1.,0.,0.));
#11557=DIRECTION('center_axis',(0.,-1.,0.));
#11558=DIRECTION('ref_axis',(1.,0.,0.));
#11559=DIRECTION('center_axis',(0.,1.,0.));
#11560=DIRECTION('ref_axis',(1.,0.,0.));
#11561=DIRECTION('',(-0.866025403784439,-0.5,-1.06057523872491E-16));
#11562=DIRECTION('center_axis',(1.92296268638356E-16,0.,-1.));
#11563=DIRECTION('ref_axis',(-1.,0.,-1.92296268638356E-16));
#11564=DIRECTION('',(0.,1.,0.));
#11565=DIRECTION('',(0.,1.,0.));
#11566=DIRECTION('center_axis',(-0.866025403784439,0.,-0.5));
#11567=DIRECTION('ref_axis',(-0.5,0.,0.866025403784439));
#11568=DIRECTION('',(0.,1.,0.));
#11569=DIRECTION('center_axis',(-0.866025403784439,0.,0.5));
#11570=DIRECTION('ref_axis',(0.5,0.,0.866025403784439));
#11571=DIRECTION('',(0.,1.,0.));
#11572=DIRECTION('center_axis',(0.,1.,0.));
#11573=DIRECTION('ref_axis',(1.,0.,0.));
#11574=DIRECTION('center_axis',(0.,1.,0.));
#11575=DIRECTION('ref_axis',(1.,0.,0.));
#11576=DIRECTION('',(0.,-1.,0.));
#11577=DIRECTION('center_axis',(0.,1.,0.));
#11578=DIRECTION('ref_axis',(1.,0.,0.));
#11579=DIRECTION('center_axis',(-1.92296268638356E-16,0.,1.));
#11580=DIRECTION('ref_axis',(1.,0.,1.92296268638356E-16));
#11581=DIRECTION('',(0.,1.,0.));
#11582=DIRECTION('center_axis',(0.866025403784439,0.,-0.5));
#11583=DIRECTION('ref_axis',(-0.5,0.,-0.866025403784439));
#11584=DIRECTION('',(0.,1.,0.));
#11585=DIRECTION('center_axis',(0.866025403784439,0.,0.5));
#11586=DIRECTION('ref_axis',(0.5,0.,-0.866025403784439));
#11587=DIRECTION('center_axis',(0.,1.,0.));
#11588=DIRECTION('ref_axis',(1.,0.,0.));
#11589=DIRECTION('center_axis',(0.,1.,0.));
#11590=DIRECTION('ref_axis',(1.,0.,0.));
#16056=CARTESIAN_POINT('',(0.,0.,0.));
#16057=CARTESIAN_POINT('Origin',(0.,0.0584134911936118,0.));
#16058=CARTESIAN_POINT('',(-0.288675134594813,0.0590919554682611,0.5));
#16059=CARTESIAN_POINT('',(0.288675134594813,0.0590919554682611,0.5));
#16060=CARTESIAN_POINT('Ctrl Pts',(-0.288675134594813,0.0590919554682611,
0.5));
#16061=CARTESIAN_POINT('Ctrl Pts',(2.1664336991023E-12,-0.0242413778636964,
0.5));
#16062=CARTESIAN_POINT('Ctrl Pts',(0.288675134594813,0.0590919554682611,
0.5));
#16063=CARTESIAN_POINT('',(-0.577350269189626,0.0590919554682611,-7.07050159149938E-17));
#16064=CARTESIAN_POINT('Ctrl Pts',(-0.577350269189626,0.0590919554682611,
-7.07050159149938E-17));
#16065=CARTESIAN_POINT('Ctrl Pts',(-0.433012701891136,-0.0242413778636963,
0.250000000001876));
#16066=CARTESIAN_POINT('Ctrl Pts',(-0.288675134594813,0.0590919554682611,
0.5));
#16067=CARTESIAN_POINT('',(-0.475,-4.16333634234434E-17,-5.81707229594993E-17));
#16068=CARTESIAN_POINT('',(-0.576175134594813,0.0584134911936118,-7.05611034329833E-17));
#16069=CARTESIAN_POINT('Origin',(0.,0.,0.));
#16070=CARTESIAN_POINT('',(-0.288675134594813,0.0590919554682611,-0.5));
#16071=CARTESIAN_POINT('Ctrl Pts',(-0.288675134594813,0.0590919554682611,
-0.5));
#16072=CARTESIAN_POINT('Ctrl Pts',(-0.433012701893303,-0.0242413778636963,
-0.249999999998124));
#16073=CARTESIAN_POINT('Ctrl Pts',(-0.577350269189626,0.0590919554682611,
-7.07050159149938E-17));
#16074=CARTESIAN_POINT('',(0.288675134594813,0.0590919554682611,-0.5));
#16075=CARTESIAN_POINT('Ctrl Pts',(0.288675134594813,0.0590919554682611,
-0.5));
#16076=CARTESIAN_POINT('Ctrl Pts',(-2.16648921025353E-12,-0.0242413778636962,
-0.5));
#16077=CARTESIAN_POINT('Ctrl Pts',(-0.288675134594813,0.0590919554682611,
-0.5));
#16078=CARTESIAN_POINT('',(0.577350269189626,0.0590919554682611,0.));
#16079=CARTESIAN_POINT('Ctrl Pts',(0.577350269189626,0.0590919554682611,
0.));
#16080=CARTESIAN_POINT('Ctrl Pts',(0.433012701891136,-0.0242413778636963,
-0.250000000001876));
#16081=CARTESIAN_POINT('Ctrl Pts',(0.288675134594813,0.0590919554682611,
-0.5));
#16082=CARTESIAN_POINT('Ctrl Pts',(0.288675134594813,0.0590919554682611,
0.5));
#16083=CARTESIAN_POINT('Ctrl Pts',(0.433012701893303,-0.0242413778636962,
0.249999999998124));
#16084=CARTESIAN_POINT('Ctrl Pts',(0.577350269189626,0.0590919554682611,
0.));
#16085=CARTESIAN_POINT('Origin',(0.,0.461586508806388,0.));
#16086=CARTESIAN_POINT('',(-0.475,0.52,-5.81707229594993E-17));
#16087=CARTESIAN_POINT('Origin',(0.,0.52,0.));
#16088=CARTESIAN_POINT('',(-0.577350269189626,0.460908044531739,-7.07050159149938E-17));
#16089=CARTESIAN_POINT('',(-0.576175134594813,0.461586508806388,-7.05611034329833E-17));
#16090=CARTESIAN_POINT('',(-0.288675134594813,0.460908044531739,0.5));
#16091=CARTESIAN_POINT('Ctrl Pts',(-0.288675134594813,0.460908044531739,
0.5));
#16092=CARTESIAN_POINT('Ctrl Pts',(-0.433012701893303,0.544241377863696,
0.249999999998124));
#16093=CARTESIAN_POINT('Ctrl Pts',(-0.577350269189626,0.460908044531739,
-7.07050159149938E-17));
#16094=CARTESIAN_POINT('',(0.288675134594813,0.460908044531739,0.5));
#16095=CARTESIAN_POINT('Ctrl Pts',(0.288675134594813,0.460908044531739,
0.5));
#16096=CARTESIAN_POINT('Ctrl Pts',(-2.16676676600969E-12,0.544241377863697,
0.5));
#16097=CARTESIAN_POINT('Ctrl Pts',(-0.288675134594813,0.460908044531739,
0.5));
#16098=CARTESIAN_POINT('',(0.577350269189626,0.460908044531739,0.));
#16099=CARTESIAN_POINT('Ctrl Pts',(0.577350269189626,0.460908044531739,
0.));
#16100=CARTESIAN_POINT('Ctrl Pts',(0.433012701891136,0.544241377863696,
0.250000000001876));
#16101=CARTESIAN_POINT('Ctrl Pts',(0.288675134594813,0.460908044531739,
0.5));
#16102=CARTESIAN_POINT('',(0.288675134594813,0.460908044531739,-0.5));
#16103=CARTESIAN_POINT('Ctrl Pts',(0.288675134594813,0.460908044531739,
-0.5));
#16104=CARTESIAN_POINT('Ctrl Pts',(0.433012701893302,0.544241377863696,
-0.249999999998124));
#16105=CARTESIAN_POINT('Ctrl Pts',(0.577350269189626,0.460908044531739,
0.));
#16106=CARTESIAN_POINT('',(-0.288675134594813,0.460908044531739,-0.5));
#16107=CARTESIAN_POINT('Ctrl Pts',(-0.288675134594813,0.460908044531739,
-0.5));
#16108=CARTESIAN_POINT('Ctrl Pts',(2.16660023255599E-12,0.544241377863697,
-0.5));
#16109=CARTESIAN_POINT('Ctrl Pts',(0.288675134594813,0.460908044531739,
-0.5));
#16110=CARTESIAN_POINT('Ctrl Pts',(-0.577350269189626,0.460908044531739,
-7.07050159149938E-17));
#16111=CARTESIAN_POINT('Ctrl Pts',(-0.433012701891136,0.544241377863696,
-0.250000000001876));
#16112=CARTESIAN_POINT('Ctrl Pts',(-0.288675134594813,0.460908044531739,
-0.5));
#16113=CARTESIAN_POINT('Origin',(0.288675134594813,0.,-0.5));
#16114=CARTESIAN_POINT('',(-0.288675134594813,0.,-0.5));
#16115=CARTESIAN_POINT('',(0.288675134594813,0.,-0.5));
#16116=CARTESIAN_POINT('Origin',(-0.288675134594813,0.,-0.5));
#16117=CARTESIAN_POINT('',(-0.577350269189626,0.,-7.07050159149938E-17));
#16118=CARTESIAN_POINT('Origin',(-0.577350269189626,0.,-7.07050159149938E-17));
#16119=CARTESIAN_POINT('',(-0.288675134594813,0.,0.5));
#16120=CARTESIAN_POINT('Origin',(0.,0.,0.));
#16121=CARTESIAN_POINT('',(-0.25175,0.52,3.08304831685346E-17));
#16122=CARTESIAN_POINT('Origin',(0.,0.52,0.));
#16123=CARTESIAN_POINT('',(-0.25175,0.,3.08304831685346E-17));
#16124=CARTESIAN_POINT('',(-0.25175,0.,3.08304831685346E-17));
#16125=CARTESIAN_POINT('Origin',(0.,0.,0.));
#16126=CARTESIAN_POINT('Origin',(-0.288675134594813,0.,0.5));
#16127=CARTESIAN_POINT('',(0.288675134594813,0.,0.5));
#16128=CARTESIAN_POINT('Origin',(0.577350269189626,0.,0.));
#16129=CARTESIAN_POINT('',(0.577350269189626,0.,0.));
#16130=CARTESIAN_POINT('Origin',(0.288675134594813,0.,0.5));
#16131=CARTESIAN_POINT('Origin',(0.,0.52,0.));
#16132=CARTESIAN_POINT('Origin',(0.,0.,0.));
#16975=UNCERTAINTY_MEASURE_WITH_UNIT(LENGTH_MEASURE(0.001),#17047,
'DISTANCE_ACCURACY_VALUE',
'Maximum model space distance between geometric entities at asserted c
onnectivities');
#16993=UNCERTAINTY_MEASURE_WITH_UNIT(LENGTH_MEASURE(0.001),#17047,
'DISTANCE_ACCURACY_VALUE',
'Maximum model space distance between geometric entities at asserted c
onnectivities');
#17028=(
GEOMETRIC_REPRESENTATION_CONTEXT(3)
GLOBAL_UNCERTAINTY_ASSIGNED_CONTEXT((#16975))
GLOBAL_UNIT_ASSIGNED_CONTEXT((#17047,#17049,#17050))
REPRESENTATION_CONTEXT('','3D')
);
#17046=(
GEOMETRIC_REPRESENTATION_CONTEXT(3)
GLOBAL_UNCERTAINTY_ASSIGNED_CONTEXT((#16993))
GLOBAL_UNIT_ASSIGNED_CONTEXT((#17047,#17049,#17050))
REPRESENTATION_CONTEXT('','3D')
);
#17047=(
LENGTH_UNIT()
NAMED_UNIT(*)
SI_UNIT(.CENTI.,.METRE.)
);
#17049=(
NAMED_UNIT(*)
PLANE_ANGLE_UNIT()
SI_UNIT($,.RADIAN.)
);
#17050=(
NAMED_UNIT(*)
SI_UNIT($,.STERADIAN.)
SOLID_ANGLE_UNIT()
);
#17085=SHAPE_DEFINITION_REPRESENTATION(#17142,#17292);
#17142=PRODUCT_DEFINITION_SHAPE('',$,#17345);
#17292=SHAPE_REPRESENTATION('',(#9439),#17028);
#17310=PRODUCT_DEFINITION_CONTEXT('part definition',#17468,'design');
#17345=PRODUCT_DEFINITION('Hex Nut - M6','Hex Nut - M6',#17397,#17310);
#17397=PRODUCT_DEFINITION_FORMATION('',$,#17504);
#17468=APPLICATION_CONTEXT(
'Core Data for Automotive Mechanical Design Process');
#17469=PRODUCT_CONTEXT('part definition',#17468,'mechanical');
#17504=PRODUCT('Hex Nut - M6','Hex Nut - M6','Hex Nut - M6',(#17469));
#17592=COLOUR_RGB('Black',0.12,0.14,0.17);
#17593=FILL_AREA_STYLE_COLOUR('',#17592);
#17594=FILL_AREA_STYLE('',(#17593));
#17595=SURFACE_STYLE_FILL_AREA(#17594);
#17596=SURFACE_SIDE_STYLE('',(#17595));
#17597=SURFACE_STYLE_USAGE(.BOTH.,#17596);
#17598=PRESENTATION_STYLE_ASSIGNMENT((#17597));
ENDSEC;
END-ISO-10303-21;
